ISO-10303-21;
HEADER;
/* Generated by software containing ST-Developer
 * from STEP Tools, Inc. (www.steptools.com) 
 */

FILE_DESCRIPTION(
/* description */ ('PAT-091'),
/* implementation_level */ '2;1');

FILE_NAME(
/* name */ 'M4 low-profile retaining screw (12).step',
/* time_stamp */ '2026-10-27T15:34:44-07:00',
/* author */ (''),
/* organization */ (''),
/* preprocessor_version */ 'ST-DEVELOPER v20.2',
/* originating_system */ 'Autodesk Translation Framework v15.17.0.0',
/* authorisation */ '');

FILE_SCHEMA (('AUTOMOTIVE_DESIGN { 1 0 10303 214 3 1 1 }'));
ENDSEC;

DATA;
#10=MECHANICAL_DESIGN_GEOMETRIC_PRESENTATION_REPRESENTATION('',(#1066),#25100);
#846=SHAPE_REPRESENTATION_RELATIONSHIP('SRR','None',#25613,#956);
#956=ADVANCED_BREP_SHAPE_REPRESENTATION('',(#1187),#25083);
#1066=STYLED_ITEM('',(#26198),#1187);
#1187=MANIFOLD_SOLID_BREP('Body1',#13346);
#1613=FACE_BOUND('',#3972,.T.);
#2012=PLANE('',#16093);
#2013=PLANE('',#16098);
#2014=PLANE('',#16101);
#2755=FACE_OUTER_BOUND('',#3971,.T.);
#2756=FACE_OUTER_BOUND('',#3973,.T.);
#2757=FACE_OUTER_BOUND('',#3974,.T.);
#2758=FACE_OUTER_BOUND('',#3975,.T.);
#2759=FACE_OUTER_BOUND('',#3976,.T.);
#3971=EDGE_LOOP('',(#11660));
#3972=EDGE_LOOP('',(#11661));
#3973=EDGE_LOOP('',(#11662,#11663,#11664,#11665));
#3974=EDGE_LOOP('',(#11666));
#3975=EDGE_LOOP('',(#11667,#11668,#11669,#11670));
#3976=EDGE_LOOP('',(#11671));
#4826=LINE('',#24140,#5566);
#4827=LINE('',#24144,#5567);
#5566=VECTOR('',#20196,0.350000000000001);
#5567=VECTOR('',#20201,0.199999999999999);
#6242=CIRCLE('',#16094,0.350000000000001);
#6243=CIRCLE('',#16095,0.199999999999999);
#6244=CIRCLE('',#16097,0.350000000000001);
#6245=CIRCLE('',#16100,0.199999999999999);
#7275=VERTEX_POINT('',#24133);
#7276=VERTEX_POINT('',#24135);
#7277=VERTEX_POINT('',#24138);
#7278=VERTEX_POINT('',#24143);
#8765=EDGE_CURVE('',#7275,#7275,#6242,.T.);
#8766=EDGE_CURVE('',#7276,#7276,#6243,.T.);
#8767=EDGE_CURVE('',#7277,#7277,#6244,.T.);
#8768=EDGE_CURVE('',#7277,#7275,#4826,.T.);
#8769=EDGE_CURVE('',#7276,#7278,#4827,.T.);
#8770=EDGE_CURVE('',#7278,#7278,#6245,.T.);
#11660=ORIENTED_EDGE('',*,*,#8765,.F.);
#11661=ORIENTED_EDGE('',*,*,#8766,.T.);
#11662=ORIENTED_EDGE('',*,*,#8767,.F.);
#11663=ORIENTED_EDGE('',*,*,#8768,.T.);
#11664=ORIENTED_EDGE('',*,*,#8765,.T.);
#11665=ORIENTED_EDGE('',*,*,#8768,.F.);
#11666=ORIENTED_EDGE('',*,*,#8767,.T.);
#11667=ORIENTED_EDGE('',*,*,#8766,.F.);
#11668=ORIENTED_EDGE('',*,*,#8769,.T.);
#11669=ORIENTED_EDGE('',*,*,#8770,.T.);
#11670=ORIENTED_EDGE('',*,*,#8769,.F.);
#11671=ORIENTED_EDGE('',*,*,#8770,.F.);
#12382=CYLINDRICAL_SURFACE('',#16096,0.350000000000001);
#12383=CYLINDRICAL_SURFACE('',#16099,0.199999999999999);
#13122=ADVANCED_FACE('',(#2755,#1613),#2012,.F.);
#13123=ADVANCED_FACE('',(#2756),#12382,.T.);
#13124=ADVANCED_FACE('',(#2757),#2013,.T.);
#13125=ADVANCED_FACE('',(#2758),#12383,.T.);
#13126=ADVANCED_FACE('',(#2759),#2014,.F.);
#13346=CLOSED_SHELL('',(#13122,#13123,#13124,#13125,#13126));
#16092=AXIS2_PLACEMENT_3D('',#24131,#20184,#20185);
#16093=AXIS2_PLACEMENT_3D('',#24132,#20186,#20187);
#16094=AXIS2_PLACEMENT_3D('',#24134,#20188,#20189);
#16095=AXIS2_PLACEMENT_3D('',#24136,#20190,#20191);
#16096=AXIS2_PLACEMENT_3D('',#24137,#20192,#20193);
#16097=AXIS2_PLACEMENT_3D('',#24139,#20194,#20195);
#16098=AXIS2_PLACEMENT_3D('',#24141,#20197,#20198);
#16099=AXIS2_PLACEMENT_3D('',#24142,#20199,#20200);
#16100=AXIS2_PLACEMENT_3D('',#24145,#20202,#20203);
#16101=AXIS2_PLACEMENT_3D('',#24146,#20204,#20205);
#20184=DIRECTION('axis',(0.,0.,1.));
#20185=DIRECTION('refdir',(1.,0.,0.));
#20186=DIRECTION('center_axis',(0.,1.,0.));
#20187=DIRECTION('ref_axis',(1.,0.,0.));
#20188=DIRECTION('center_axis',(0.,1.,0.));
#20189=DIRECTION('ref_axis',(1.,0.,0.));
#20190=DIRECTION('center_axis',(0.,1.,0.));
#20191=DIRECTION('ref_axis',(1.,0.,0.));
#20192=DIRECTION('center_axis',(0.,1.,0.));
#20193=DIRECTION('ref_axis',(1.,0.,0.));
#20194=DIRECTION('center_axis',(0.,1.,0.));
#20195=DIRECTION('ref_axis',(1.,0.,0.));
#20196=DIRECTION('',(0.,-1.,0.));
#20197=DIRECTION('center_axis',(0.,1.,0.));
#20198=DIRECTION('ref_axis',(1.,0.,0.));
#20199=DIRECTION('center_axis',(0.,1.,0.));
#20200=DIRECTION('ref_axis',(1.,0.,0.));
#20201=DIRECTION('',(0.,-1.,0.));
#20202=DIRECTION('center_axis',(0.,1.,0.));
#20203=DIRECTION('ref_axis',(1.,0.,0.));
#20204=DIRECTION('center_axis',(0.,1.,0.));
#20205=DIRECTION('ref_axis',(1.,0.,0.));
#24131=CARTESIAN_POINT('',(0.,0.,0.));
#24132=CARTESIAN_POINT('Origin',(20.6730642762322,8.3,9.30814754519511));
#24133=CARTESIAN_POINT('',(20.3230642762322,8.3,9.30814754519511));
#24134=CARTESIAN_POINT('Origin',(20.6730642762322,8.3,9.30814754519511));
#24135=CARTESIAN_POINT('',(20.4730642762322,8.3,9.30814754519511));
#24136=CARTESIAN_POINT('Origin',(20.6730642762322,8.3,9.30814754519511));
#24137=CARTESIAN_POINT('Origin',(20.6730642762322,8.3,9.30814754519511));
#24138=CARTESIAN_POINT('',(20.3230642762322,8.4,9.30814754519511));
#24139=CARTESIAN_POINT('Origin',(20.6730642762322,8.4,9.30814754519511));
#24140=CARTESIAN_POINT('',(20.3230642762322,8.3,9.30814754519511));
#24141=CARTESIAN_POINT('Origin',(20.6730642762322,8.4,9.30814754519511));
#24142=CARTESIAN_POINT('Origin',(20.6730642762322,7.6,9.30814754519511));
#24143=CARTESIAN_POINT('',(20.4730642762322,7.6,9.30814754519511));
#24144=CARTESIAN_POINT('',(20.4730642762322,7.6,9.30814754519511));
#24145=CARTESIAN_POINT('Origin',(20.6730642762322,7.6,9.30814754519511));
#24146=CARTESIAN_POINT('Origin',(20.6730642762322,7.6,9.30814754519511));
#24962=UNCERTAINTY_MEASURE_WITH_UNIT(LENGTH_MEASURE(0.001),#25101,
'DISTANCE_ACCURACY_VALUE',
'Maximum model space distance between geometric entities at asserted c
onnectivities');
#24979=UNCERTAINTY_MEASURE_WITH_UNIT(LENGTH_MEASURE(0.001),#25101,
'DISTANCE_ACCURACY_VALUE',
'Maximum model space distance between geometric entities at asserted c
onnectivities');
#25083=(
GEOMETRIC_REPRESENTATION_CONTEXT(3)
GLOBAL_UNCERTAINTY_ASSIGNED_CONTEXT((#24962))
GLOBAL_UNIT_ASSIGNED_CONTEXT((#25101,#25103,#25104))
REPRESENTATION_CONTEXT('','3D')
);
#25100=(
GEOMETRIC_REPRESENTATION_CONTEXT(3)
GLOBAL_UNCERTAINTY_ASSIGNED_CONTEXT((#24979))
GLOBAL_UNIT_ASSIGNED_CONTEXT((#25101,#25103,#25104))
REPRESENTATION_CONTEXT('','3D')
);
#25101=(
LENGTH_UNIT()
NAMED_UNIT(*)
SI_UNIT(.CENTI.,.METRE.)
);
#25103=(
NAMED_UNIT(*)
PLANE_ANGLE_UNIT()
SI_UNIT($,.RADIAN.)
);
#25104=(
NAMED_UNIT(*)
SI_UNIT($,.STERADIAN.)
SOLID_ANGLE_UNIT()
);
#25208=SHAPE_DEFINITION_REPRESENTATION(#25402,#25613);
#25402=PRODUCT_DEFINITION_SHAPE('',$,#25734);
#25613=SHAPE_REPRESENTATION('',(#16092),#25083);
#25630=PRODUCT_DEFINITION_CONTEXT('part definition',#25992,'design');
#25734=PRODUCT_DEFINITION('M4 low-profile retaining screw (12)',
'M4 low-profile retaining screw (12)',#25854,#25630);
#25854=PRODUCT_DEFINITION_FORMATION('',$,#26097);
#25992=APPLICATION_CONTEXT(
'Core Data for Automotive Mechanical Design Process');
#25993=PRODUCT_CONTEXT('part definition',#25992,'mechanical');
#26097=PRODUCT('M4 low-profile retaining screw (12)',
'M4 low-profile retaining screw (12)','M4 low-profile retaining screw (12)',
(#25993));
#26192=COLOUR_RGB('Black',0.12,0.14,0.17);
#26193=FILL_AREA_STYLE_COLOUR('',#26192);
#26194=FILL_AREA_STYLE('',(#26193));
#26195=SURFACE_STYLE_FILL_AREA(#26194);
#26196=SURFACE_SIDE_STYLE('',(#26195));
#26197=SURFACE_STYLE_USAGE(.BOTH.,#26196);
#26198=PRESENTATION_STYLE_ASSIGNMENT((#26197));
ENDSEC;
END-ISO-10303-21;
